ISO-10303-21;
HEADER;
FILE_DESCRIPTION (('STEP AP214'),
    '1' );
FILE_NAME ('isolation positive negative.step',
    '2026-10-05T20:10:51',
    ( '' ),
    ( '' ),
    'SwSTEP 2.0',
    'SolidWorks 2020',
    '' );
FILE_SCHEMA (( 'AUTOMOTIVE_DESIGN' ));
ENDSEC;

DATA;
#218=LINE ( 'NONE', #116204, #61046 ) ;
#794=EDGE_LOOP ( 'NONE', ( #170295, #136868, #121989, #212162, #31787, #181573, #75016, #98751 ) ) ;
#1086=EDGE_CURVE ( 'NONE', #188607, #206477, #202400, .T. ) ;
#1147=DIRECTION ( 'NONE',  ( 0.000000000000000000, 0.000000000000000000, 1.000000000000000000 ) ) ;
#1962=CYLINDRICAL_SURFACE ( 'NONE', #101371, 2.000000000000000000 ) ;
#1986=CARTESIAN_POINT ( 'NONE',  ( 1.836970198721030181E-16, 7.500000000000000000, 1.500000000000000222 ) ) ;
#2364=ORIENTED_EDGE ( 'NONE', *, *, #150402, .T. ) ;
#2458=ORIENTED_EDGE ( 'NONE', *, *, #64463, .F. ) ;
#2603=CARTESIAN_POINT ( 'NONE',  ( 4.000000000000012434, 4.999999999999997335, -0.7500000000000006661 ) ) ;
#2981=VECTOR ( 'NONE', #30547, 1000.000000000000000 ) ;
#3032=DIRECTION ( 'NONE',  ( -0.000000000000000000, -1.000000000000000000, 0.000000000000000000 ) ) ;
#3179=CARTESIAN_POINT ( 'NONE',  ( 4.000000000000022204, 5.999999999999998224, 2.024999999999999023 ) ) ;
#3215=AXIS2_PLACEMENT_3D ( 'NONE', #186064, #37700, #103776 ) ;
#3845=EDGE_LOOP ( 'NONE', ( #61817, #107068, #146519, #143070, #69421, #145271, #154020 ) ) ;
#4064=CARTESIAN_POINT ( 'NONE',  ( 4.000000000000012434, 4.999999999999997335, -1.214306433183764966E-14 ) ) ;
#4099=CARTESIAN_POINT ( 'NONE',  ( 0.000000000000000000, 5.499999999999998224, 0.000000000000000000 ) ) ;
#4254=LINE ( 'NONE', #106106, #38900 ) ;
#4424=CARTESIAN_POINT ( 'NONE',  ( 4.000000000000012434, 4.999999999999997335, 0.7500000000000006661 ) ) ;
#4489=PLANE ( 'NONE',  #154520 ) ;
#4753=VERTEX_POINT ( 'NONE', #40541 ) ;
#4983=LINE ( 'NONE', #107935, #196145 ) ;
#5124=( NAMED_UNIT ( * ) PLANE_ANGLE_UNIT ( ) SI_UNIT ( $, .RADIAN. ) );
#5367=DIRECTION ( 'NONE',  ( -0.000000000000000000, -1.000000000000000000, 0.000000000000000000 ) ) ;
#5753=CARTESIAN_POINT ( 'NONE',  ( 0.000000000000000000, 5.999999999999998224, 0.000000000000000000 ) ) ;
#5816=FACE_BOUND ( 'NONE', #9308, .T. ) ;
#5896=PLANE ( 'NONE',  #184540 ) ;
#6689=MECHANICAL_DESIGN_GEOMETRIC_PRESENTATION_REPRESENTATION('',(#183110),#96735);
#6910=EDGE_LOOP ( 'NONE', ( #121706, #135092, #177174, #22707 ) ) ;
#6914=ORIENTED_EDGE ( 'NONE', *, *, #191961, .F. ) ;
#6957=DIRECTION ( 'NONE',  ( 0.000000000000000000, 0.000000000000000000, 1.000000000000000000 ) ) ;
#7455=ORIENTED_EDGE ( 'NONE', *, *, #45482, .T. ) ;
#7624=CARTESIAN_POINT ( 'NONE',  ( -1.854049621773892653, 4.999999999999997335, -0.7500000000000015543 ) ) ;
#7753=ORIENTED_EDGE ( 'NONE', *, *, #182547, .F. ) ;
#7909=ORIENTED_EDGE ( 'NONE', *, *, #145707, .T. ) ;
#8096=CARTESIAN_POINT ( 'NONE',  ( 0.000000000000000000, 7.500000000000000000, 0.000000000000000000 ) ) ;
#8119=CARTESIAN_POINT ( 'NONE',  ( 3.449547071718269020, 5.499999999999998224, 2.024999999999999023 ) ) ;
#8437=VECTOR ( 'NONE', #174577, 1000.000000000000000 ) ;
#8753=CARTESIAN_POINT ( 'NONE',  ( -1.299038105676657340, 5.999999999999998224, 0.7500000000000006661 ) ) ;
#8934=DIRECTION ( 'NONE',  ( 0.000000000000000000, 0.000000000000000000, -1.000000000000000000 ) ) ;
#9308=EDGE_LOOP ( 'NONE', ( #171057, #177648 ) ) ;
#9426=VECTOR ( 'NONE', #174333, 1000.000000000000000 ) ;
#9667=CARTESIAN_POINT ( 'NONE',  ( 3.929058411375439874, 5.999999999999998224, 0.7500000000000006661 ) ) ;
#9759=VECTOR ( 'NONE', #150361, 1000.000000000000000 ) ;
#10693=DIRECTION ( 'NONE',  ( 0.000000000000000000, 0.000000000000000000, 1.000000000000000000 ) ) ;
#10696=PRODUCT_DEFINITION_FORMATION_WITH_SPECIFIED_SOURCE ( 'ANY', '', #60975, .NOT_KNOWN. ) ;
#10990=FACE_OUTER_BOUND ( 'NONE', #173079, .T. ) ;
#11011=ORIENTED_EDGE ( 'NONE', *, *, #204911, .F. ) ;
#11168=ADVANCED_FACE ( 'NONE', ( #21522 ), #37814, .F. ) ;
#11226=VECTOR ( 'NONE', #131183, 1000.000000000000000 ) ;
#11614=VERTEX_POINT ( 'NONE', #207764 ) ;
#11640=EDGE_CURVE ( 'NONE', #105851, #112521, #34587, .T. ) ;
#11886=EDGE_CURVE ( 'NONE', #122450, #88429, #25414, .T. ) ;
#12030=CARTESIAN_POINT ( 'NONE',  ( 0.000000000000000000, 5.499999999999998224, 0.000000000000000000 ) ) ;
#12150=ADVANCED_FACE ( 'NONE', ( #40626 ), #139185, .F. ) ;
#12506=DIRECTION ( 'NONE',  ( 0.000000000000000000, 0.000000000000000000, 1.000000000000000000 ) ) ;
#12508=AXIS2_PLACEMENT_3D ( 'NONE', #43016, #39793, #142656 ) ;
#12605=FACE_OUTER_BOUND ( 'NONE', #146731, .T. ) ;
#12810=DIRECTION ( 'NONE',  ( -1.000000000000000000, 0.000000000000000000, 0.000000000000000000 ) ) ;
#13090=DIRECTION ( 'NONE',  ( 0.000000000000000000, 0.000000000000000000, 1.000000000000000000 ) ) ;
#13249=DIRECTION ( 'NONE',  ( 0.000000000000000000, 0.000000000000000000, 1.000000000000000000 ) ) ;
#13658=ADVANCED_FACE ( 'NONE', ( #26575 ), #54818, .F. ) ;
#13676=DIRECTION ( 'NONE',  ( 0.000000000000000000, 0.000000000000000000, 1.000000000000000000 ) ) ;
#13943=ORIENTED_EDGE ( 'NONE', *, *, #136186, .T. ) ;
#14433=EDGE_LOOP ( 'NONE', ( #135450, #17726, #27003, #177400 ) ) ;
#14623=VERTEX_POINT ( 'NONE', #8753 ) ;
#15160=CARTESIAN_POINT ( 'NONE',  ( 4.000000000000012434, 6.499999999999999112, -0.7500000000000006661 ) ) ;
#15193=FACE_OUTER_BOUND ( 'NONE', #134382, .T. ) ;
#15306=CARTESIAN_POINT ( 'NONE',  ( 0.000000000000000000, 6.499999999999999112, 0.000000000000000000 ) ) ;
#15734=DIRECTION ( 'NONE',  ( 0.000000000000000000, 1.000000000000000000, 0.000000000000000000 ) ) ;
#15855=EDGE_LOOP ( 'NONE', ( #70311, #146301, #171842, #87400 ) ) ;
#16386=CARTESIAN_POINT ( 'NONE',  ( 4.000000000000001776, 5.999999999999998224, -2.024999999999999911 ) ) ;
#16565=DIRECTION ( 'NONE',  ( -0.000000000000000000, -1.000000000000000000, -0.000000000000000000 ) ) ;
#16695=VECTOR ( 'NONE', #209626, 1000.000000000000000 ) ;
#17301=CARTESIAN_POINT ( 'NONE',  ( 4.000000000000012434, 0.000000000000000000, 0.7500000000000006661 ) ) ;
#17406=ADVANCED_FACE ( 'NONE', ( #106349 ), #4489, .F. ) ;
#17627=CARTESIAN_POINT ( 'NONE',  ( 3.929058411375439874, -1.000000000000000888, -0.7500000000000006661 ) ) ;
#17726=ORIENTED_EDGE ( 'NONE', *, *, #99278, .F. ) ;
#17785=CARTESIAN_POINT ( 'NONE',  ( 1.854049621773927514, 4.999999999999997335, 0.7500000000000006661 ) ) ;
#18187=( NAMED_UNIT ( * ) SI_UNIT ( $, .STERADIAN. ) SOLID_ANGLE_UNIT ( ) );
#18336=FILL_AREA_STYLE ('',( #51930 ) ) ;
#18505=AXIS2_PLACEMENT_3D ( 'NONE', #212000, #128727, #63640 ) ;
#18637=DIRECTION ( 'NONE',  ( 0.000000000000000000, 1.000000000000000000, 0.000000000000000000 ) ) ;
#19707=PLANE ( 'NONE',  #53151 ) ;
#20109=EDGE_CURVE ( 'NONE', #53056, #32144, #109365, .T. ) ;
#20260=EDGE_CURVE ( 'NONE', #68331, #206477, #44305, .T. ) ;
#20466=( NAMED_UNIT ( * ) PLANE_ANGLE_UNIT ( ) SI_UNIT ( $, .RADIAN. ) );
#21154=AXIS2_PLACEMENT_3D ( 'NONE', #33832, #136688, #70569 ) ;
#21379=SURFACE_SIDE_STYLE ('',( #133063 ) ) ;
#21522=FACE_OUTER_BOUND ( 'NONE', #3845, .T. ) ;
#21866=CIRCLE ( 'NONE', #129152, 1.500000000000000222 ) ;
#22139=FACE_OUTER_BOUND ( 'NONE', #132445, .T. ) ;
#22354=ORIENTED_EDGE ( 'NONE', *, *, #23613, .T. ) ;
#22391=AXIS2_PLACEMENT_3D ( 'NONE', #142876, #208878, #107202 ) ;
#22525=CARTESIAN_POINT ( 'NONE',  ( -3.449547071718257030, 5.999999999999998224, 2.025000000000002576 ) ) ;
#22707=ORIENTED_EDGE ( 'NONE', *, *, #142558, .T. ) ;
#23131=AXIS2_PLACEMENT_3D ( 'NONE', #23437, #88473, #24506 ) ;
#23412=ORIENTED_EDGE ( 'NONE', *, *, #37914, .T. ) ;
#23437=CARTESIAN_POINT ( 'NONE',  ( 0.000000000000000000, 4.999999999999997335, 0.000000000000000000 ) ) ;
#23568=AXIS2_PLACEMENT_3D ( 'NONE', #28306, #93337, #159373 ) ;
#23613=EDGE_CURVE ( 'NONE', #58716, #180119, #138195, .T. ) ;
#23963=DIRECTION ( 'NONE',  ( 0.000000000000000000, 0.000000000000000000, 1.000000000000000000 ) ) ;
#24506=DIRECTION ( 'NONE',  ( 0.000000000000000000, 0.000000000000000000, 1.000000000000000000 ) ) ;
#24845=CARTESIAN_POINT ( 'NONE',  ( 0.000000000000000000, 5.499999999999998224, 0.000000000000000000 ) ) ;
#25083=CARTESIAN_POINT ( 'NONE',  ( -1.854049621773913525, 5.499999999999998224, 0.7500000000000006661 ) ) ;
#25374=DIRECTION ( 'NONE',  ( 0.000000000000000000, 1.000000000000000000, 0.000000000000000000 ) ) ;
#25414=LINE ( 'NONE', #127285, #65646 ) ;
#25526=DIRECTION ( 'NONE',  ( -0.000000000000000000, -1.000000000000000000, 0.000000000000000000 ) ) ;
#26575=FACE_OUTER_BOUND ( 'NONE', #198875, .T. ) ;
#26828=VECTOR ( 'NONE', #15734, 1000.000000000000000 ) ;
#26947=PLANE ( 'NONE',  #155153 ) ;
#26960=CARTESIAN_POINT ( 'NONE',  ( 4.000000000000012434, 5.999999999999998224, -0.7500000000000006661 ) ) ;
#27003=ORIENTED_EDGE ( 'NONE', *, *, #174535, .T. ) ;
#28306=CARTESIAN_POINT ( 'NONE',  ( 4.000000000000012434, 0.000000000000000000, -0.7500000000000006661 ) ) ;
#28381=ORIENTED_EDGE ( 'NONE', *, *, #89939, .F. ) ;
#28854=FACE_OUTER_BOUND ( 'NONE', #111653, .T. ) ;
#29297=CARTESIAN_POINT ( 'NONE',  ( -3.449547071718236158, 5.499999999999998224, -2.024999999999992806 ) ) ;
#29395=AXIS2_PLACEMENT_3D ( 'NONE', #32284, #46412, #112528 ) ;
#29580=EDGE_CURVE ( 'NONE', #14623, #126234, #4254, .T. ) ;
#29949=CARTESIAN_POINT ( 'NONE',  ( 0.000000000000000000, -1.000000000000000888, 0.000000000000000000 ) ) ;
#30547=DIRECTION ( 'NONE',  ( -1.000000000000000000, 0.000000000000000000, 0.000000000000000000 ) ) ;
#31415=CARTESIAN_POINT ( 'NONE',  ( -1.299038105676657340, 6.499999999999999112, 0.7500000000000006661 ) ) ;
#31534=CARTESIAN_POINT ( 'NONE',  ( -3.929058411375401683, 5.499999999999998224, -0.7500000000000006661 ) ) ;
#31653=DIRECTION ( 'NONE',  ( 0.000000000000000000, 1.000000000000000000, 0.000000000000000000 ) ) ;
#31718=CARTESIAN_POINT ( 'NONE',  ( 0.000000000000000000, 4.999999999999997335, 0.000000000000000000 ) ) ;
#31787=ORIENTED_EDGE ( 'NONE', *, *, #156896, .F. ) ;
#32030=ORIENTED_EDGE ( 'NONE', *, *, #56710, .F. ) ;
#32144=VERTEX_POINT ( 'NONE', #17785 ) ;
#32247=EDGE_CURVE ( 'NONE', #207943, #84441, #133741, .T. ) ;
#32284=CARTESIAN_POINT ( 'NONE',  ( 0.000000000000000000, 7.500000000000000000, 0.000000000000000000 ) ) ;
#32644=ORIENTED_EDGE ( 'NONE', *, *, #20109, .T. ) ;
#32966=CARTESIAN_POINT ( 'NONE',  ( -1.854049621773892653, 5.499999999999998224, -0.7500000000000015543 ) ) ;
#33110=CARTESIAN_POINT ( 'NONE',  ( 0.000000000000000000, 5.499999999999998224, -2.000000000000000000 ) ) ;
#33297=ORIENTED_EDGE ( 'NONE', *, *, #20260, .F. ) ;
#33598=ORIENTED_EDGE ( 'NONE', *, *, #144618, .T. ) ;
#33702=DIRECTION ( 'NONE',  ( 0.000000000000000000, 1.000000000000000000, 0.000000000000000000 ) ) ;
#33832=CARTESIAN_POINT ( 'NONE',  ( 0.000000000000000000, 0.000000000000000000, 0.000000000000000000 ) ) ;
#34299=ORIENTED_EDGE ( 'NONE', *, *, #142583, .F. ) ;
#34325=VERTEX_POINT ( 'NONE', #35366 ) ;
#34587=CIRCLE ( 'NONE', #86395, 4.000000000000000000 ) ;
#35254=DIRECTION ( 'NONE',  ( 0.000000000000000000, 0.000000000000000000, 1.000000000000000000 ) ) ;
#35304=EDGE_LOOP ( 'NONE', ( #196519, #11011, #51581, #23412 ) ) ;
#35366=CARTESIAN_POINT ( 'NONE',  ( -3.929058411375426108, 4.999999999999997335, 0.7499999999999988898 ) ) ;
#35899=CIRCLE ( 'NONE', #156984, 2.000000000000000000 ) ;
#35961=CARTESIAN_POINT ( 'NONE',  ( 4.000000000000012434, 6.499999999999999112, -1.214306433183764966E-14 ) ) ;
#36149=( GEOMETRIC_REPRESENTATION_CONTEXT ( 3 ) GLOBAL_UNCERTAINTY_ASSIGNED_CONTEXT ( ( #123539 ) ) GLOBAL_UNIT_ASSIGNED_CONTEXT ( ( #102807, #20466, #101735 ) ) REPRESENTATION_CONTEXT ( 'NONE', 'WORKASPACE' ) );
#37289=CARTESIAN_POINT ( 'NONE',  ( 3.929058411375439874, -1.000000000000000888, 0.7500000000000006661 ) ) ;
#37700=DIRECTION ( 'NONE',  ( 0.000000000000000000, 1.000000000000000000, 0.000000000000000000 ) ) ;
#37814=PLANE ( 'NONE',  #89976 ) ;
#37843=VERTEX_POINT ( 'NONE', #205713 ) ;
#37914=EDGE_CURVE ( 'NONE', #108790, #58716, #122443, .T. ) ;
#38294=ORIENTED_EDGE ( 'NONE', *, *, #56710, .T. ) ;
#38351=PLANE ( 'NONE',  #173358 ) ;
#38900=VECTOR ( 'NONE', #86605, 1000.000000000000000 ) ;
#39793=DIRECTION ( 'NONE',  ( 0.000000000000000000, 1.000000000000000000, 0.000000000000000000 ) ) ;
#39835=UNCERTAINTY_MEASURE_WITH_UNIT (LENGTH_MEASURE( 1.000000000000000082E-05 ), #53915, 'distance_accuracy_value', 'NONE');
#40303=AXIS2_PLACEMENT_3D ( 'NONE', #29949, #146916, #13676 ) ;
#40503=CARTESIAN_POINT ( 'NONE',  ( 0.000000000000000000, 0.000000000000000000, 0.000000000000000000 ) ) ;
#40541=CARTESIAN_POINT ( 'NONE',  ( -3.929058411375426108, 5.499999999999998224, 0.7499999999999988898 ) ) ;
#40626=FACE_OUTER_BOUND ( 'NONE', #204531, .T. ) ;
#40716=DIRECTION ( 'NONE',  ( -1.000000000000000000, 0.000000000000000000, 0.000000000000000000 ) ) ;
#40876=LINE ( 'NONE', #41947, #161264 ) ;
#40891=APPLICATION_CONTEXT ( 'automotive_design' ) ;
#41469=CARTESIAN_POINT ( 'NONE',  ( 4.000000000000012434, 0.000000000000000000, -0.7500000000000006661 ) ) ;
#41601=EDGE_LOOP ( 'NONE', ( #151332, #153689 ) ) ;
#41947=CARTESIAN_POINT ( 'NONE',  ( 4.000000000000012434, 5.499999999999998224, 0.7500000000000006661 ) ) ;
#42154=ORIENTED_EDGE ( 'NONE', *, *, #23613, .F. ) ;
#42198=LINE ( 'NONE', #125642, #9426 ) ;
#42393=VERTEX_POINT ( 'NONE', #60910 ) ;
#42407=ADVANCED_FACE ( 'NONE', ( #160545 ), #194104, .F. ) ;
#42535=VECTOR ( 'NONE', #166839, 1000.000000000000000 ) ;
#42658=DIRECTION ( 'NONE',  ( -1.000000000000000000, 0.000000000000000000, 0.000000000000000000 ) ) ;
#42816=VECTOR ( 'NONE', #133631, 1000.000000000000000 ) ;
#43016=CARTESIAN_POINT ( 'NONE',  ( 0.000000000000000000, 5.499999999999998224, 0.000000000000000000 ) ) ;
#43091=ORIENTED_EDGE ( 'NONE', *, *, #59071, .T. ) ;
#43415=ORIENTED_EDGE ( 'NONE', *, *, #37914, .F. ) ;
#43515=DIRECTION ( 'NONE',  ( 0.000000000000000000, 0.000000000000000000, -1.000000000000000000 ) ) ;
#43517=FACE_OUTER_BOUND ( 'NONE', #86542, .T. ) ;
#43758=LINE ( 'NONE', #191028, #164151 ) ;
#43957=ORIENTED_EDGE ( 'NONE', *, *, #179963, .F. ) ;
#44080=VECTOR ( 'NONE', #137560, 1000.000000000000000 ) ;
#44124=EDGE_CURVE ( 'NONE', #79317, #34325, #62016, .T. ) ;
#44305=LINE ( 'NONE', #190524, #68209 ) ;
#44355=CARTESIAN_POINT ( 'NONE',  ( 3.929058411375439874, 6.499999999999999112, 0.7500000000000006661 ) ) ;
#44359=CIRCLE ( 'NONE', #127469, 4.000000000000000000 ) ;
#44580=PLANE ( 'NONE',  #23568 ) ;
#44711=DIRECTION ( 'NONE',  ( 0.000000000000000000, 1.000000000000000000, 0.000000000000000000 ) ) ;
#45127=DIRECTION ( 'NONE',  ( 0.000000000000000000, 1.000000000000000000, -8.673617379884026597E-16 ) ) ;
#45482=EDGE_CURVE ( 'NONE', #69052, #207943, #201712, .T. ) ;
#45609=EDGE_CURVE ( 'NONE', #166283, #120928, #198014, .T. ) ;
#45691=ADVANCED_FACE ( 'NONE', ( #203333 ), #54986, .F. ) ;
#45782=CARTESIAN_POINT ( 'NONE',  ( 0.000000000000000000, 5.999999999999998224, 0.000000000000000000 ) ) ;
#46152=EDGE_CURVE ( 'NONE', #180119, #125532, #139334, .T. ) ;
#46194=LINE ( 'NONE', #80811, #150713 ) ;
#46412=DIRECTION ( 'NONE',  ( -0.000000000000000000, -1.000000000000000000, 0.000000000000000000 ) ) ;
#46438=DIRECTION ( 'NONE',  ( 0.000000000000000000, 1.000000000000000000, 0.000000000000000000 ) ) ;
#47092=ORIENTED_EDGE ( 'NONE', *, *, #191961, .T. ) ;
#47273=SHAPE_REPRESENTATION ( 'isolation positive negative', ( #200407 ), #151904 ) ;
#47384=DIRECTION ( 'NONE',  ( 0.000000000000000000, 0.000000000000000000, 1.000000000000000000 ) ) ;
#47458=AXIS2_PLACEMENT_3D ( 'NONE', #212185, #48654, #134191 ) ;
#47492=PLANE ( 'NONE',  #160813 ) ;
#47745=PLANE ( 'NONE',  #73268 ) ;
#48167=ORIENTED_EDGE ( 'NONE', *, *, #145607, .F. ) ;
#48178=DIRECTION ( 'NONE',  ( -0.000000000000000000, -1.000000000000000000, -0.000000000000000000 ) ) ;
#48225=AXIS2_PLACEMENT_3D ( 'NONE', #62012, #44711, #13249 ) ;
#48575=DIRECTION ( 'NONE',  ( 0.000000000000000000, 0.000000000000000000, 1.000000000000000000 ) ) ;
#48654=DIRECTION ( 'NONE',  ( 0.000000000000000000, -1.000000000000000000, 0.000000000000000000 ) ) ;
#48666=EDGE_CURVE ( 'NONE', #34325, #4753, #112780, .T. ) ;
#48924=CIRCLE ( 'NONE', #197636, 1.500000000000000222 ) ;
#49683=VERTEX_POINT ( 'NONE', #137794 ) ;
#50070=CIRCLE ( 'NONE', #105443, 2.000000000000000000 ) ;
#50110=VECTOR ( 'NONE', #73566, 1000.000000000000000 ) ;
#50284=LINE ( 'NONE', #32966, #149799 ) ;
#50335=VERTEX_POINT ( 'NONE', #72702 ) ;
#51118=ORIENTED_EDGE ( 'NONE', *, *, #116869, .T. ) ;
#51532=DIRECTION ( 'NONE',  ( 0.000000000000000000, 1.000000000000000000, 0.000000000000000000 ) ) ;
#51581=ORIENTED_EDGE ( 'NONE', *, *, #56226, .T. ) ;
#51930=FILL_AREA_STYLE_COLOUR ( '', #74666 ) ;
#52114=DIRECTION ( 'NONE',  ( 0.000000000000000000, 0.000000000000000000, 1.000000000000000000 ) ) ;
#52979=SURFACE_SIDE_STYLE ('',( #150506 ) ) ;
#52990=CARTESIAN_POINT ( 'NONE',  ( 4.000000000000012434, 5.499999999999998224, -1.214306433183764966E-14 ) ) ;
#53056=VERTEX_POINT ( 'NONE', #74028 ) ;
#53151=AXIS2_PLACEMENT_3D ( 'NONE', #35961, #18637, #134574 ) ;
#53769=LINE ( 'NONE', #152334, #141450 ) ;
#53915=( LENGTH_UNIT ( ) NAMED_UNIT ( * ) SI_UNIT ( .MILLI., .METRE. ) );
#54249=CIRCLE ( 'NONE', #23131, 4.000000000000000000 ) ;
#54354=DIRECTION ( 'NONE',  ( -1.000000000000000000, 0.000000000000000000, 0.000000000000000000 ) ) ;
#54602=CARTESIAN_POINT ( 'NONE',  ( 0.000000000000000000, 5.499999999999998224, 0.000000000000000000 ) ) ;
#54818=PLANE ( 'NONE',  #93068 ) ;
#54935=DIRECTION ( 'NONE',  ( -0.000000000000000000, -1.000000000000000000, -0.000000000000000000 ) ) ;
#54986=PLANE ( 'NONE',  #96209 ) ;
#55021=DIRECTION ( 'NONE',  ( 0.000000000000000000, 0.000000000000000000, -1.000000000000000000 ) ) ;
#56226=EDGE_CURVE ( 'NONE', #142172, #108790, #82771, .T. ) ;
#56261=CARTESIAN_POINT ( 'NONE',  ( 4.000000000000001776, 5.499999999999998224, -2.024999999999999023 ) ) ;
#56710=EDGE_CURVE ( 'NONE', #96482, #65271, #105044, .T. ) ;
#56775=CARTESIAN_POINT ( 'NONE',  ( 3.929058411375439874, 4.999999999999997335, -0.7500000000000006661 ) ) ;
#56814=CARTESIAN_POINT ( 'NONE',  ( 0.000000000000000000, 5.499999999999998224, 0.000000000000000000 ) ) ;
#57361=CYLINDRICAL_SURFACE ( 'NONE', #113249, 2.000000000000000000 ) ;
#57493=PRODUCT_DEFINITION ( 'UNKNOWN', '', #10696, #187288 ) ;
#57553=EDGE_LOOP ( 'NONE', ( #63025, #179576, #141493, #87386 ) ) ;
#57972=LINE ( 'NONE', #88349, #118308 ) ;
#58695=DIRECTION ( 'NONE',  ( 0.000000000000000000, 0.000000000000000000, 1.000000000000000000 ) ) ;
#58716=VERTEX_POINT ( 'NONE', #137496 ) ;
#59071=EDGE_CURVE ( 'NONE', #14623, #50335, #48924, .T. ) ;
#59485=LINE ( 'NONE', #155934, #44080 ) ;
#59877=VECTOR ( 'NONE', #81248, 1000.000000000000000 ) ;
#60389=CARTESIAN_POINT ( 'NONE',  ( 4.000000000000012434, 5.999999999999998224, 0.7500000000000006661 ) ) ;
#60607=EDGE_CURVE ( 'NONE', #50335, #159873, #166659, .T. ) ;
#60790=DIRECTION ( 'NONE',  ( 0.000000000000000000, 0.000000000000000000, 1.000000000000000000 ) ) ;
#60910=CARTESIAN_POINT ( 'NONE',  ( 1.854049621773927514, 5.499999999999998224, 0.7500000000000006661 ) ) ;
#60975=PRODUCT ( 'isolation positive negative', 'isolation positive negative', '', ( #213993 ) ) ;
#61046=VECTOR ( 'NONE', #183267, 1000.000000000000000 ) ;
#61125=DIRECTION ( 'NONE',  ( -1.000000000000000000, 0.000000000000000000, 0.000000000000000000 ) ) ;
#61653=CARTESIAN_POINT ( 'NONE',  ( 1.299038105676669330, 6.499999999999999112, -0.7500000000000006661 ) ) ;
#61817=ORIENTED_EDGE ( 'NONE', *, *, #195348, .F. ) ;
#61829=CARTESIAN_POINT ( 'NONE',  ( -3.449547071718257030, 5.499999999999998224, 2.025000000000002576 ) ) ;
#62012=CARTESIAN_POINT ( 'NONE',  ( 0.000000000000000000, 5.999999999999998224, 0.000000000000000000 ) ) ;
#62016=CIRCLE ( 'NONE', #3215, 4.000000000000000000 ) ;
#62197=DIRECTION ( 'NONE',  ( 0.000000000000000000, 1.000000000000000000, 0.000000000000000000 ) ) ;
#62634=FACE_OUTER_BOUND ( 'NONE', #105617, .T. ) ;
#63025=ORIENTED_EDGE ( 'NONE', *, *, #136902, .F. ) ;
#63592=VECTOR ( 'NONE', #48178, 1000.000000000000000 ) ;
#63640=DIRECTION ( 'NONE',  ( 0.000000000000000000, 0.000000000000000000, 1.000000000000000000 ) ) ;
#64051=LINE ( 'NONE', #116050, #118488 ) ;
#64178=ORIENTED_EDGE ( 'NONE', *, *, #174535, .F. ) ;
#64463=EDGE_CURVE ( 'NONE', #205093, #188607, #179823, .T. ) ;
#65011=CARTESIAN_POINT ( 'NONE',  ( 4.000000000000012434, 4.999999999999997335, -1.214306433183764966E-14 ) ) ;
#65271=VERTEX_POINT ( 'NONE', #9667 ) ;
#65646=VECTOR ( 'NONE', #61125, 1000.000000000000000 ) ;
#66921=FILL_AREA_STYLE ('',( #186026 ) ) ;
#67108=DIRECTION ( 'NONE',  ( -1.000000000000000000, 0.000000000000000000, 0.000000000000000000 ) ) ;
#67292=ORIENTED_EDGE ( 'NONE', *, *, #179963, .T. ) ;
#67644=ORIENTED_EDGE ( 'NONE', *, *, #144618, .F. ) ;
#67833=CIRCLE ( 'NONE', #12508, 4.000000000000000000 ) ;
#67961=ORIENTED_EDGE ( 'NONE', *, *, #149140, .T. ) ;
#68209=VECTOR ( 'NONE', #90927, 1000.000000000000000 ) ;
#68331=VERTEX_POINT ( 'NONE', #88761 ) ;
#68335=ORIENTED_EDGE ( 'NONE', *, *, #32247, .F. ) ;
#68982=COLOUR_RGB ( '', 0.40784314, 0.44705882, 0.49803922) ;
#69052=VERTEX_POINT ( 'NONE', #140128 ) ;
#69065=SURFACE_STYLE_USAGE ( .BOTH. , #21379 ) ;
#69421=ORIENTED_EDGE ( 'NONE', *, *, #181457, .T. ) ;
#69503=ORIENTED_EDGE ( 'NONE', *, *, #100213, .F. ) ;
#69981=DIRECTION ( 'NONE',  ( -1.000000000000000000, 0.000000000000000000, 0.000000000000000000 ) ) ;
#69992=AXIS2_PLACEMENT_3D ( 'NONE', #149562, #200417, #1147 ) ;
#70156=ORIENTED_EDGE ( 'NONE', *, *, #73625, .T. ) ;
#70198=EDGE_CURVE ( 'NONE', #32144, #84441, #35899, .T. ) ;
#70311=ORIENTED_EDGE ( 'NONE', *, *, #201380, .F. ) ;
#70569=DIRECTION ( 'NONE',  ( 0.000000000000000000, 0.000000000000000000, 1.000000000000000000 ) ) ;
#70991=DIRECTION ( 'NONE',  ( -0.000000000000000000, -1.000000000000000000, 0.000000000000000000 ) ) ;
#71199=( NAMED_UNIT ( * ) SI_UNIT ( $, .STERADIAN. ) SOLID_ANGLE_UNIT ( ) );
#71979=VERTEX_POINT ( 'NONE', #22525 ) ;
#72119=ORIENTED_EDGE ( 'NONE', *, *, #175034, .F. ) ;
#72496=CARTESIAN_POINT ( 'NONE',  ( 4.000000000000012434, 5.999999999999998224, -1.214306433183764966E-14 ) ) ;
#72702=CARTESIAN_POINT ( 'NONE',  ( 1.836970198721030181E-16, 5.999999999999998224, 1.500000000000000222 ) ) ;
#72968=FACE_OUTER_BOUND ( 'NONE', #41601, .T. ) ;
#72997=ORIENTED_EDGE ( 'NONE', *, *, #181457, .F. ) ;
#73268=AXIS2_PLACEMENT_3D ( 'NONE', #65011, #164665, #83395 ) ;
#73306=ORIENTED_EDGE ( 'NONE', *, *, #181995, .F. ) ;
#73336=DIRECTION ( 'NONE',  ( -1.000000000000000000, 0.000000000000000000, 0.000000000000000000 ) ) ;
#73422=CIRCLE ( 'NONE', #156462, 2.000000000000000000 ) ;
#73535=DIRECTION ( 'NONE',  ( 0.000000000000000000, 1.000000000000000000, 0.000000000000000000 ) ) ;
#73566=DIRECTION ( 'NONE',  ( -1.000000000000000000, 0.000000000000000000, 0.000000000000000000 ) ) ;
#73625=EDGE_CURVE ( 'NONE', #37843, #34325, #132372, .T. ) ;
#74028=CARTESIAN_POINT ( 'NONE',  ( 3.929058411375439874, 4.999999999999997335, 0.7500000000000006661 ) ) ;
#74058=DIRECTION ( 'NONE',  ( 0.000000000000000000, 1.000000000000000000, 0.000000000000000000 ) ) ;
#74666=COLOUR_RGB ( '', 0.40784314, 0.44705882, 0.49803922) ;
#74947=DIRECTION ( 'NONE',  ( 0.000000000000000000, 1.000000000000000000, 0.000000000000000000 ) ) ;
#75016=ORIENTED_EDGE ( 'NONE', *, *, #70198, .F. ) ;
#75048=ORIENTED_EDGE ( 'NONE', *, *, #11640, .F. ) ;
#75159=CARTESIAN_POINT ( 'NONE',  ( -1.854049621773892653, 5.499999999999998224, -0.7500000000000015543 ) ) ;
#75480=EDGE_CURVE ( 'NONE', #42393, #32144, #57972, .T. ) ;
#75664=CARTESIAN_POINT ( 'NONE',  ( 1.299038105676669330, 6.499999999999999112, 0.7500000000000006661 ) ) ;
#75727=DIRECTION ( 'NONE',  ( -1.000000000000000000, 0.000000000000000000, 0.000000000000000000 ) ) ;
#76457=ORIENTED_EDGE ( 'NONE', *, *, #89939, .T. ) ;
#76502=ORIENTED_EDGE ( 'NONE', *, *, #92489, .T. ) ;
#76581=ORIENTED_EDGE ( 'NONE', *, *, #44124, .F. ) ;
#76641=LINE ( 'NONE', #60389, #99104 ) ;
#76871=ORIENTED_EDGE ( 'NONE', *, *, #174801, .T. ) ;
#77275=ORIENTED_EDGE ( 'NONE', *, *, #1086, .F. ) ;
#77359=DIRECTION ( 'NONE',  ( 0.000000000000000000, 1.000000000000000000, 0.000000000000000000 ) ) ;
#77505=EDGE_LOOP ( 'NONE', ( #171097, #162671, #166585, #149003 ) ) ;
#77594=PLANE ( 'NONE',  #140058 ) ;
#77846=DIRECTION ( 'NONE',  ( -1.000000000000000000, 0.000000000000000000, 0.000000000000000000 ) ) ;
#78101=DIRECTION ( 'NONE',  ( 0.000000000000000000, 1.000000000000000000, 0.000000000000000000 ) ) ;
#78209=CIRCLE ( 'NONE', #109360, 1.500000000000000222 ) ;
#78448=ORIENTED_EDGE ( 'NONE', *, *, #135735, .T. ) ;
#79317=VERTEX_POINT ( 'NONE', #84952 ) ;
#79391=VERTEX_POINT ( 'NONE', #29297 ) ;
#80202=CARTESIAN_POINT ( 'NONE',  ( 4.000000000000012434, 6.499999999999999112, 0.7500000000000006661 ) ) ;
#80363=DIRECTION ( 'NONE',  ( 0.000000000000000000, 0.000000000000000000, -1.000000000000000000 ) ) ;
#80450=ORIENTED_EDGE ( 'NONE', *, *, #56226, .F. ) ;
#80503=CARTESIAN_POINT ( 'NONE',  ( 1.854049621773927514, 5.499999999999998224, -0.7500000000000006661 ) ) ;
#80575=ADVANCED_FACE ( 'NONE', ( #167695 ), #1962, .T. ) ;
#80811=CARTESIAN_POINT ( 'NONE',  ( -3.449547071718236158, -1.000000000000000888, -2.024999999999992806 ) ) ;
#81248=DIRECTION ( 'NONE',  ( -1.000000000000000000, 0.000000000000000000, 0.000000000000000000 ) ) ;
#81384=LINE ( 'NONE', #94464, #191503 ) ;
#81820=CARTESIAN_POINT ( 'NONE',  ( -3.449547071718257030, -1.000000000000000888, 2.025000000000002576 ) ) ;
#82154=ORIENTED_EDGE ( 'NONE', *, *, #204535, .T. ) ;
#82311=CIRCLE ( 'NONE', #158405, 1.500000000000000222 ) ;
#82358=CARTESIAN_POINT ( 'NONE',  ( 0.000000000000000000, 5.999999999999998224, -1.500000000000000222 ) ) ;
#82581=EDGE_CURVE ( 'NONE', #68331, #71979, #174227, .T. ) ;
#82771=LINE ( 'NONE', #196536, #63592 ) ;
#83395=DIRECTION ( 'NONE',  ( 0.000000000000000000, 0.000000000000000000, 1.000000000000000000 ) ) ;
#83440=LINE ( 'NONE', #117077, #42535 ) ;
#83482=AXIS2_PLACEMENT_3D ( 'NONE', #54602, #74058, #186725 ) ;
#83806=ADVANCED_FACE ( 'NONE', ( #22139 ), #5896, .T. ) ;
#84441=VERTEX_POINT ( 'NONE', #139985 ) ;
#84952=CARTESIAN_POINT ( 'NONE',  ( -3.929058411375401683, 4.999999999999997335, -0.7500000000000006661 ) ) ;
#84971=DIRECTION ( 'NONE',  ( -0.000000000000000000, -1.000000000000000000, -0.000000000000000000 ) ) ;
#85178=DIRECTION ( 'NONE',  ( 0.000000000000000000, 1.000000000000000000, 0.000000000000000000 ) ) ;
#85284=EDGE_LOOP ( 'NONE', ( #163882, #187306, #112248, #125825, #38294, #67961, #67644 ) ) ;
#85472=CIRCLE ( 'NONE', #47458, 1.500000000000000222 ) ;
#85656=VERTEX_POINT ( 'NONE', #207118 ) ;
#85741=CARTESIAN_POINT ( 'NONE',  ( 0.000000000000000000, 0.000000000000000000, -1.500000000000000222 ) ) ;
#85977=DIRECTION ( 'NONE',  ( 0.000000000000000000, 1.000000000000000000, 0.000000000000000000 ) ) ;
#86395=AXIS2_PLACEMENT_3D ( 'NONE', #199887, #51532, #35254 ) ;
#86472=DIRECTION ( 'NONE',  ( -0.000000000000000000, -1.000000000000000000, 0.000000000000000000 ) ) ;
#86542=EDGE_LOOP ( 'NONE', ( #108396, #7455, #156740, #148132 ) ) ;
#86578=VERTEX_POINT ( 'NONE', #138431 ) ;
#86605=DIRECTION ( 'NONE',  ( 0.000000000000000000, 1.000000000000000000, -0.000000000000000000 ) ) ;
#87386=ORIENTED_EDGE ( 'NONE', *, *, #20109, .F. ) ;
#87400=ORIENTED_EDGE ( 'NONE', *, *, #88823, .T. ) ;
#87416=CARTESIAN_POINT ( 'NONE',  ( 4.000000000000012434, 5.999999999999998224, -0.7500000000000006661 ) ) ;
#87633=DIRECTION ( 'NONE',  ( 0.000000000000000000, 1.000000000000000000, 0.000000000000000000 ) ) ;
#88172=DIRECTION ( 'NONE',  ( 0.000000000000000000, 0.000000000000000000, 1.000000000000000000 ) ) ;
#88349=CARTESIAN_POINT ( 'NONE',  ( 1.854049621773927514, 5.499999999999998224, 0.7500000000000006661 ) ) ;
#88429=VERTEX_POINT ( 'NONE', #61829 ) ;
#88473=DIRECTION ( 'NONE',  ( 0.000000000000000000, 1.000000000000000000, 0.000000000000000000 ) ) ;
#88556=EDGE_CURVE ( 'NONE', #126234, #206477, #152649, .T. ) ;
#88702=CIRCLE ( 'NONE', #189028, 4.000000000000000000 ) ;
#88761=CARTESIAN_POINT ( 'NONE',  ( -3.929058411375426108, 5.999999999999998224, 0.7499999999999988898 ) ) ;
#88823=EDGE_CURVE ( 'NONE', #96482, #71979, #104998, .T. ) ;
#88960=DIRECTION ( 'NONE',  ( 0.000000000000000000, 1.000000000000000000, 0.000000000000000000 ) ) ;
#88981=ADVANCED_BREP_SHAPE_REPRESENTATION ( '', ( #91223, #200407 ), #151904 ) ;
#89287=ORIENTED_EDGE ( 'NONE', *, *, #129217, .T. ) ;
#89325=CARTESIAN_POINT ( 'NONE',  ( 0.000000000000000000, 5.499999999999998224, 0.000000000000000000 ) ) ;
#89882=DIRECTION ( 'NONE',  ( 0.000000000000000000, 0.000000000000000000, -1.000000000000000000 ) ) ;
#89894=ORIENTED_EDGE ( 'NONE', *, *, #201380, .T. ) ;
#89939=EDGE_CURVE ( 'NONE', #86578, #112521, #154550, .T. ) ;
#89976=AXIS2_PLACEMENT_3D ( 'NONE', #52990, #87633, #185107 ) ;
#90927=DIRECTION ( 'NONE',  ( 0.000000000000000000, 1.000000000000000000, 0.000000000000000000 ) ) ;
#91223=MANIFOLD_SOLID_BREP ( 'Cut-Extrude2', #126141 ) ;
#91522=AXIS2_PLACEMENT_3D ( 'NONE', #12030, #78101, #13090 ) ;
#91869=VECTOR ( 'NONE', #165721, 1000.000000000000000 ) ;
#92262=CARTESIAN_POINT ( 'NONE',  ( 0.000000000000000000, 5.999999999999998224, 0.000000000000000000 ) ) ;
#92489=EDGE_CURVE ( 'NONE', #79317, #213798, #190690, .T. ) ;
#93055=DIRECTION ( 'NONE',  ( 0.000000000000000000, 1.000000000000000000, 0.000000000000000000 ) ) ;
#93068=AXIS2_PLACEMENT_3D ( 'NONE', #172851, #107908, #40716 ) ;
#93309=ORIENTED_EDGE ( 'NONE', *, *, #100213, .T. ) ;
#93337=DIRECTION ( 'NONE',  ( 0.000000000000000000, 0.000000000000000000, -1.000000000000000000 ) ) ;
#93790=ORIENTED_EDGE ( 'NONE', *, *, #135040, .F. ) ;
#93969=DIRECTION ( 'NONE',  ( 0.000000000000000000, 0.000000000000000000, 1.000000000000000000 ) ) ;
#94313=VERTEX_POINT ( 'NONE', #75159 ) ;
#94464=CARTESIAN_POINT ( 'NONE',  ( 4.000000000000012434, 5.999999999999998224, 0.7500000000000006661 ) ) ;
#95216=CARTESIAN_POINT ( 'NONE',  ( 0.000000000000000000, 0.000000000000000000, 0.000000000000000000 ) ) ;
#95578=EDGE_CURVE ( 'NONE', #205093, #126234, #78209, .T. ) ;
#95580=CARTESIAN_POINT ( 'NONE',  ( 4.000000000000022204, 0.000000000000000000, 2.024999999999999023 ) ) ;
#95888=AXIS2_PLACEMENT_3D ( 'NONE', #210011, #208944, #160220 ) ;
#96209=AXIS2_PLACEMENT_3D ( 'NONE', #4064, #77359, #127271 ) ;
#96227=CARTESIAN_POINT ( 'NONE',  ( -3.929058411375401683, 6.499999999999999112, -0.7500000000000006661 ) ) ;
#96482=VERTEX_POINT ( 'NONE', #117748 ) ;
#96662=ORIENTED_EDGE ( 'NONE', *, *, #118355, .F. ) ;
#96735=( GEOMETRIC_REPRESENTATION_CONTEXT ( 3 ) GLOBAL_UNCERTAINTY_ASSIGNED_CONTEXT ( ( #39835 ) ) GLOBAL_UNIT_ASSIGNED_CONTEXT ( ( #53915, #5124, #71199 ) ) REPRESENTATION_CONTEXT ( 'NONE', 'WORKASPACE' ) );
#97099=CYLINDRICAL_SURFACE ( 'NONE', #40303, 4.000000000000000000 ) ;
#97271=CIRCLE ( 'NONE', #83482, 4.000000000000000000 ) ;
#97596=ORIENTED_EDGE ( 'NONE', *, *, #163875, .T. ) ;
#97896=EDGE_CURVE ( 'NONE', #205873, #156566, #218, .T. ) ;
#98349=CYLINDRICAL_SURFACE ( 'NONE', #29395, 1.500000000000000222 ) ;
#98500=AXIS2_PLACEMENT_3D ( 'NONE', #114360, #160911, #12506 ) ;
#98751=ORIENTED_EDGE ( 'NONE', *, *, #75480, .F. ) ;
#99104=VECTOR ( 'NONE', #126553, 1000.000000000000000 ) ;
#99278=EDGE_CURVE ( 'NONE', #175693, #99756, #171024, .T. ) ;
#99645=FACE_OUTER_BOUND ( 'NONE', #6910, .T. ) ;
#99756=VERTEX_POINT ( 'NONE', #75664 ) ;
#99947=AXIS2_PLACEMENT_3D ( 'NONE', #56814, #25374, #203035 ) ;
#100213=EDGE_CURVE ( 'NONE', #53056, #207943, #54249, .T. ) ;
#100920=ORIENTED_EDGE ( 'NONE', *, *, #20260, .T. ) ;
#100955=FACE_OUTER_BOUND ( 'NONE', #14433, .T. ) ;
#101076=CARTESIAN_POINT ( 'NONE',  ( -1.299038105676632915, 7.500000000000000000, -0.7500000000000006661 ) ) ;
#101187=DIRECTION ( 'NONE',  ( -1.000000000000000000, 0.000000000000000000, 0.000000000000000000 ) ) ;
#101371=AXIS2_PLACEMENT_3D ( 'NONE', #4099, #3032, #55021 ) ;
#101735=( NAMED_UNIT ( * ) SI_UNIT ( $, .STERADIAN. ) SOLID_ANGLE_UNIT ( ) );
#101776=ORIENTED_EDGE ( 'NONE', *, *, #46152, .T. ) ;
#102226=DIRECTION ( 'NONE',  ( 0.000000000000000000, 0.000000000000000000, 1.000000000000000000 ) ) ;
#102807=( LENGTH_UNIT ( ) NAMED_UNIT ( * ) SI_UNIT ( .MILLI., .METRE. ) );
#103776=DIRECTION ( 'NONE',  ( 0.000000000000000000, 0.000000000000000000, 1.000000000000000000 ) ) ;
#104451=APPLICATION_CONTEXT ( 'automotive_design' ) ;
#104717=ORIENTED_EDGE ( 'NONE', *, *, #129217, .F. ) ;
#104998=LINE ( 'NONE', #3179, #206082 ) ;
#105044=CIRCLE ( 'NONE', #163798, 4.000000000000000000 ) ;
#105443=AXIS2_PLACEMENT_3D ( 'NONE', #212686, #62197, #198562 ) ;
#105484=CIRCLE ( 'NONE', #22391, 1.500000000000000222 ) ;
#105617=EDGE_LOOP ( 'NONE', ( #143072, #33598, #188078, #148435, #132571, #22354, #101776, #13943 ) ) ;
#105851=VERTEX_POINT ( 'NONE', #213106 ) ;
#106083=DIRECTION ( 'NONE',  ( -1.000000000000000000, 0.000000000000000000, 0.000000000000000000 ) ) ;
#106106=CARTESIAN_POINT ( 'NONE',  ( -1.299038105676657340, 7.500000000000000000, 0.7500000000000006661 ) ) ;
#106191=CARTESIAN_POINT ( 'NONE',  ( 3.929058411375439874, 6.499999999999999112, -0.7500000000000006661 ) ) ;
#106349=FACE_OUTER_BOUND ( 'NONE', #182227, .T. ) ;
#106967=ORIENTED_EDGE ( 'NONE', *, *, #175034, .T. ) ;
#107068=ORIENTED_EDGE ( 'NONE', *, *, #11886, .T. ) ;
#107082=CARTESIAN_POINT ( 'NONE',  ( 0.000000000000000000, 6.499999999999999112, 0.000000000000000000 ) ) ;
#107202=DIRECTION ( 'NONE',  ( 0.000000000000000000, 0.000000000000000000, -1.000000000000000000 ) ) ;
#107691=DIRECTION ( 'NONE',  ( 0.000000000000000000, 1.000000000000000000, 0.000000000000000000 ) ) ;
#107908=DIRECTION ( 'NONE',  ( 0.000000000000000000, 0.000000000000000000, -1.000000000000000000 ) ) ;
#107935=CARTESIAN_POINT ( 'NONE',  ( 4.000000000000012434, 5.499999999999998224, -0.7500000000000006661 ) ) ;
#108107=AXIS2_PLACEMENT_3D ( 'NONE', #31718, #147600, #182203 ) ;
#108128=PLANE ( 'NONE',  #135438 ) ;
#108396=ORIENTED_EDGE ( 'NONE', *, *, #198949, .F. ) ;
#108790=VERTEX_POINT ( 'NONE', #194651 ) ;
#109242=VECTOR ( 'NONE', #54935, 1000.000000000000000 ) ;
#109360=AXIS2_PLACEMENT_3D ( 'NONE', #107082, #176299, #206639 ) ;
#109365=LINE ( 'NONE', #206776, #196275 ) ;
#109576=ORIENTED_EDGE ( 'NONE', *, *, #97896, .T. ) ;
#111470=DIRECTION ( 'NONE',  ( 0.000000000000000000, 0.000000000000000000, -1.000000000000000000 ) ) ;
#111483=DIRECTION ( 'NONE',  ( -1.000000000000000000, 0.000000000000000000, 0.000000000000000000 ) ) ;
#111653=EDGE_LOOP ( 'NONE', ( #78448, #47092, #148101, #184320 ) ) ;
#111829=EDGE_CURVE ( 'NONE', #99756, #144460, #21866, .T. ) ;
#112248=ORIENTED_EDGE ( 'NONE', *, *, #82581, .T. ) ;
#112521=VERTEX_POINT ( 'NONE', #148490 ) ;
#112528=DIRECTION ( 'NONE',  ( 0.000000000000000000, 0.000000000000000000, -1.000000000000000000 ) ) ;
#112556=AXIS2_PLACEMENT_3D ( 'NONE', #128060, #74947, #58695 ) ;
#112780=LINE ( 'NONE', #211259, #204734 ) ;
#113249=AXIS2_PLACEMENT_3D ( 'NONE', #24845, #5367, #89882 ) ;
#113466=EDGE_LOOP ( 'NONE', ( #93790, #72997, #162677, #150802, #89287, #43957, #109576, #195157 ) ) ;
#113938=ORIENTED_EDGE ( 'NONE', *, *, #29580, .F. ) ;
#114049=VECTOR ( 'NONE', #75727, 1000.000000000000000 ) ;
#114360=CARTESIAN_POINT ( 'NONE',  ( 0.000000000000000000, 5.499999999999998224, 0.000000000000000000 ) ) ;
#114990=DIRECTION ( 'NONE',  ( -0.000000000000000000, -1.000000000000000000, 0.000000000000000000 ) ) ;
#115025=DIRECTION ( 'NONE',  ( 0.000000000000000000, 0.000000000000000000, 1.000000000000000000 ) ) ;
#115063=CIRCLE ( 'NONE', #108107, 2.000000000000000000 ) ;
#115177=ORIENTED_EDGE ( 'NONE', *, *, #46152, .F. ) ;
#115324=ORIENTED_EDGE ( 'NONE', *, *, #145607, .T. ) ;
#115525=SHAPE_DEFINITION_REPRESENTATION ( #126764, #47273 ) ;
#115705=CIRCLE ( 'NONE', #98500, 2.000000000000000000 ) ;
#116050=CARTESIAN_POINT ( 'NONE',  ( 1.299038105676669330, 7.500000000000000000, 0.7500000000000006661 ) ) ;
#116056=AXIS2_PLACEMENT_3D ( 'NONE', #15306, #33702, #115025 ) ;
#116204=CARTESIAN_POINT ( 'NONE',  ( 0.000000000000000000, 5.499999999999998224, -2.000000000000000000 ) ) ;
#116672=DIRECTION ( 'NONE',  ( 0.000000000000000000, 0.000000000000000000, 1.000000000000000000 ) ) ;
#116833=( LENGTH_UNIT ( ) NAMED_UNIT ( * ) SI_UNIT ( .MILLI., .METRE. ) );
#116869=EDGE_CURVE ( 'NONE', #94313, #213798, #43758, .T. ) ;
#117077=CARTESIAN_POINT ( 'NONE',  ( 1.299038105676669330, 7.500000000000000000, -0.7500000000000006661 ) ) ;
#117748=CARTESIAN_POINT ( 'NONE',  ( 3.449547071718269020, 5.999999999999998224, 2.024999999999999023 ) ) ;
#118153=ORIENTED_EDGE ( 'NONE', *, *, #135735, .F. ) ;
#118308=VECTOR ( 'NONE', #70991, 1000.000000000000000 ) ;
#118355=EDGE_CURVE ( 'NONE', #194084, #79317, #144234, .T. ) ;
#118488=VECTOR ( 'NONE', #114990, 1000.000000000000000 ) ;
#118655=EDGE_CURVE ( 'NONE', #37843, #160336, #173510, .T. ) ;
#119115=PRESENTATION_STYLE_ASSIGNMENT (( #184039 ) ) ;
#119720=VECTOR ( 'NONE', #150288, 1000.000000000000000 ) ;
#119995=ORIENTED_EDGE ( 'NONE', *, *, #209914, .T. ) ;
#120388=ORIENTED_EDGE ( 'NONE', *, *, #70198, .T. ) ;
#120415=ADVANCED_FACE ( 'NONE', ( #28854 ), #77594, .T. ) ;
#120496=DIRECTION ( 'NONE',  ( 0.000000000000000000, 1.000000000000000000, 0.000000000000000000 ) ) ;
#120640=PLANE ( 'NONE',  #140521 ) ;
#120928=VERTEX_POINT ( 'NONE', #186552 ) ;
#121111=ADVANCED_FACE ( 'NONE', ( #10990 ), #174607, .F. ) ;
#121706=ORIENTED_EDGE ( 'NONE', *, *, #48666, .F. ) ;
#121989=ORIENTED_EDGE ( 'NONE', *, *, #174645, .T. ) ;
#122055=CARTESIAN_POINT ( 'NONE',  ( -1.299038105676632915, 6.499999999999999112, -0.7500000000000006661 ) ) ;
#122240=UNCERTAINTY_MEASURE_WITH_UNIT (LENGTH_MEASURE( 1.000000000000000082E-05 ), #116833, 'distance_accuracy_value', 'NONE');
#122346=AXIS2_PLACEMENT_3D ( 'NONE', #45782, #31653, #146486 ) ;
#122443=LINE ( 'NONE', #26960, #114049 ) ;
#122450=VERTEX_POINT ( 'NONE', #8119 ) ;
#123539=UNCERTAINTY_MEASURE_WITH_UNIT (LENGTH_MEASURE( 1.000000000000000082E-05 ), #102807, 'distance_accuracy_value', 'NONE');
#123630=CIRCLE ( 'NONE', #95888, 1.500000000000000222 ) ;
#123672=CARTESIAN_POINT ( 'NONE',  ( -3.929058411375401683, -1.000000000000000888, -0.7500000000000006661 ) ) ;
#123786=ADVANCED_FACE ( 'NONE', ( #189820 ), #120640, .T. ) ;
#124197=LINE ( 'NONE', #189103, #153647 ) ;
#124426=VECTOR ( 'NONE', #111483, 1000.000000000000000 ) ;
#125460=CARTESIAN_POINT ( 'NONE',  ( 4.000000000000012434, 6.499999999999999112, -1.214306433183764966E-14 ) ) ;
#125531=FACE_OUTER_BOUND ( 'NONE', #178334, .T. ) ;
#125532=VERTEX_POINT ( 'NONE', #85741 ) ;
#125642=CARTESIAN_POINT ( 'NONE',  ( 3.449547071718269020, -1.000000000000000888, 2.024999999999999023 ) ) ;
#125825=ORIENTED_EDGE ( 'NONE', *, *, #88823, .F. ) ;
#125868=ORIENTED_EDGE ( 'NONE', *, *, #133443, .T. ) ;
#126141=CLOSED_SHELL ( 'NONE', ( #12150, #80575, #17406, #177874, #133711, #168316, #136448, #166027, #202760, #123786, #13658, #211476, #42407, #11168, #45691, #121111, #120415, #83806, #185742, #172089, #145525, #164115, #196170, #132795, #136347 ) ) ;
#126234=VERTEX_POINT ( 'NONE', #31415 ) ;
#126553=DIRECTION ( 'NONE',  ( -1.000000000000000000, 0.000000000000000000, 0.000000000000000000 ) ) ;
#126764=PRODUCT_DEFINITION_SHAPE ( 'NONE', 'NONE',  #57493 ) ;
#126949=DIRECTION ( 'NONE',  ( 0.000000000000000000, 1.000000000000000000, 0.000000000000000000 ) ) ;
#127271=DIRECTION ( 'NONE',  ( 0.000000000000000000, 0.000000000000000000, 1.000000000000000000 ) ) ;
#127285=CARTESIAN_POINT ( 'NONE',  ( 4.000000000000022204, 5.499999999999998224, 2.024999999999999023 ) ) ;
#127469=AXIS2_PLACEMENT_3D ( 'NONE', #135612, #120496, #23963 ) ;
#127513=DIRECTION ( 'NONE',  ( 0.000000000000000000, -8.673617379884026597E-16, -1.000000000000000000 ) ) ;
#127593=ORIENTED_EDGE ( 'NONE', *, *, #95578, .T. ) ;
#128060=CARTESIAN_POINT ( 'NONE',  ( 4.000000000000012434, 5.499999999999998224, -1.214306433183764966E-14 ) ) ;
#128727=DIRECTION ( 'NONE',  ( 0.000000000000000000, 1.000000000000000000, 0.000000000000000000 ) ) ;
#129128=VECTOR ( 'NONE', #101187, 1000.000000000000000 ) ;
#129152=AXIS2_PLACEMENT_3D ( 'NONE', #179635, #46438, #48575 ) ;
#129217=EDGE_CURVE ( 'NONE', #194084, #94313, #50284, .T. ) ;
#129643=MECHANICAL_DESIGN_GEOMETRIC_PRESENTATION_REPRESENTATION('',(#130111),#36149);
#129764=CARTESIAN_POINT ( 'NONE',  ( 0.000000000000000000, 0.000000000000000000, 0.000000000000000000 ) ) ;
#129883=CARTESIAN_POINT ( 'NONE',  ( 4.000000000000012434, 5.499999999999998224, 0.7500000000000006661 ) ) ;
#130111=STYLED_ITEM ( 'NONE', ( #119115 ), #91223 ) ;
#131183=DIRECTION ( 'NONE',  ( -0.000000000000000000, -1.000000000000000000, 0.000000000000000000 ) ) ;
#131908=ORIENTED_EDGE ( 'NONE', *, *, #171344, .T. ) ;
#132002=DIRECTION ( 'NONE',  ( 0.000000000000000000, 0.000000000000000000, 1.000000000000000000 ) ) ;
#132372=LINE ( 'NONE', #4424, #163094 ) ;
#132445=EDGE_LOOP ( 'NONE', ( #42154, #43415, #106967, #82154, #213937, #28381, #146685 ) ) ;
#132571=ORIENTED_EDGE ( 'NONE', *, *, #178101, .T. ) ;
#132706=CARTESIAN_POINT ( 'NONE',  ( 1.836970198721030181E-16, 0.000000000000000000, 1.500000000000000222 ) ) ;
#132736=LINE ( 'NONE', #81820, #26828 ) ;
#132795=ADVANCED_FACE ( 'NONE', ( #125531 ), #141741, .T. ) ;
#133063=SURFACE_STYLE_FILL_AREA ( #66921 ) ;
#133443=EDGE_CURVE ( 'NONE', #194084, #37843, #115063, .T. ) ;
#133631=DIRECTION ( 'NONE',  ( 0.000000000000000000, 1.000000000000000000, -0.000000000000000000 ) ) ;
#133711=ADVANCED_FACE ( 'NONE', ( #100955 ), #19707, .T. ) ;
#133741=LINE ( 'NONE', #2603, #129128 ) ;
#134191=DIRECTION ( 'NONE',  ( 0.000000000000000000, 0.000000000000000000, -1.000000000000000000 ) ) ;
#134382=EDGE_LOOP ( 'NONE', ( #69503, #32644, #120388, #68335 ) ) ;
#134574=DIRECTION ( 'NONE',  ( 0.000000000000000000, 0.000000000000000000, 1.000000000000000000 ) ) ;
#135040=EDGE_CURVE ( 'NONE', #213592, #85656, #147380, .T. ) ;
#135092=ORIENTED_EDGE ( 'NONE', *, *, #73625, .F. ) ;
#135438=AXIS2_PLACEMENT_3D ( 'NONE', #125460, #208738, #93969 ) ;
#135450=ORIENTED_EDGE ( 'NONE', *, *, #111829, .F. ) ;
#135612=CARTESIAN_POINT ( 'NONE',  ( 0.000000000000000000, 5.499999999999998224, 0.000000000000000000 ) ) ;
#135735=EDGE_CURVE ( 'NONE', #120928, #79391, #192633, .T. ) ;
#135752=AXIS2_PLACEMENT_3D ( 'NONE', #167502, #85178, #116672 ) ;
#136186=EDGE_CURVE ( 'NONE', #125532, #159873, #105484, .T. ) ;
#136347=ADVANCED_FACE ( 'NONE', ( #62634 ), #98349, .F. ) ;
#136448=ADVANCED_FACE ( 'NONE', ( #181708 ), #47492, .F. ) ;
#136607=ORIENTED_EDGE ( 'NONE', *, *, #198949, .T. ) ;
#136688=DIRECTION ( 'NONE',  ( 0.000000000000000000, 1.000000000000000000, 0.000000000000000000 ) ) ;
#136857=ORIENTED_EDGE ( 'NONE', *, *, #60607, .T. ) ;
#136868=ORIENTED_EDGE ( 'NONE', *, *, #135040, .T. ) ;
#136902=EDGE_CURVE ( 'NONE', #49683, #53056, #137268, .T. ) ;
#137268=LINE ( 'NONE', #203288, #109242 ) ;
#137496=CARTESIAN_POINT ( 'NONE',  ( 1.299038105676669330, 5.999999999999998224, -0.7500000000000006661 ) ) ;
#137560=DIRECTION ( 'NONE',  ( 0.000000000000000000, 1.000000000000000000, 0.000000000000000000 ) ) ;
#137794=CARTESIAN_POINT ( 'NONE',  ( 3.929058411375439874, 5.499999999999998224, 0.7500000000000006661 ) ) ;
#138195=CIRCLE ( 'NONE', #48225, 1.500000000000000222 ) ;
#138431=CARTESIAN_POINT ( 'NONE',  ( -1.299038105676632915, 5.999999999999998224, -0.7500000000000006661 ) ) ;
#138543=CARTESIAN_POINT ( 'NONE',  ( 4.000000000000012434, 6.499999999999999112, 0.7500000000000006661 ) ) ;
#139185=CYLINDRICAL_SURFACE ( 'NONE', #152111, 1.500000000000000222 ) ;
#139334=LINE ( 'NONE', #171816, #16695 ) ;
#139985=CARTESIAN_POINT ( 'NONE',  ( 1.854049621773927514, 4.999999999999997335, -0.7500000000000006661 ) ) ;
#140058=AXIS2_PLACEMENT_3D ( 'NONE', #143717, #127513, #45127 ) ;
#140128=CARTESIAN_POINT ( 'NONE',  ( 3.929058411375439874, 5.499999999999998224, -0.7500000000000006661 ) ) ;
#140521=AXIS2_PLACEMENT_3D ( 'NONE', #41469, #8934, #190875 ) ;
#141038=FACE_OUTER_BOUND ( 'NONE', #35304, .T. ) ;
#141237=ORIENTED_EDGE ( 'NONE', *, *, #99278, .T. ) ;
#141450=VECTOR ( 'NONE', #69981, 1000.000000000000000 ) ;
#141493=ORIENTED_EDGE ( 'NONE', *, *, #75480, .T. ) ;
#141741=CYLINDRICAL_SURFACE ( 'NONE', #18505, 4.000000000000000000 ) ;
#141788=DIRECTION ( 'NONE',  ( 0.000000000000000000, 0.000000000000000000, 1.000000000000000000 ) ) ;
#142172=VERTEX_POINT ( 'NONE', #106191 ) ;
#142558=EDGE_CURVE ( 'NONE', #160336, #4753, #40876, .T. ) ;
#142583=EDGE_CURVE ( 'NONE', #79391, #213798, #67833, .T. ) ;
#142656=DIRECTION ( 'NONE',  ( 0.000000000000000000, 0.000000000000000000, 1.000000000000000000 ) ) ;
#142876=CARTESIAN_POINT ( 'NONE',  ( 0.000000000000000000, 0.000000000000000000, 0.000000000000000000 ) ) ;
#143070=ORIENTED_EDGE ( 'NONE', *, *, #142558, .F. ) ;
#143072=ORIENTED_EDGE ( 'NONE', *, *, #60607, .F. ) ;
#143275=DIRECTION ( 'NONE',  ( -1.000000000000000000, 0.000000000000000000, 0.000000000000000000 ) ) ;
#143717=CARTESIAN_POINT ( 'NONE',  ( 4.000000000000001776, -3.469446951953614189E-15, -2.024999999999994582 ) ) ;
#144234=LINE ( 'NONE', #209156, #8437 ) ;
#144244=DIRECTION ( 'NONE',  ( -1.000000000000000000, 0.000000000000000000, 0.000000000000000000 ) ) ;
#144281=VECTOR ( 'NONE', #106083, 1000.000000000000000 ) ;
#144460=VERTEX_POINT ( 'NONE', #61653 ) ;
#144618=EDGE_CURVE ( 'NONE', #50335, #11614, #123630, .T. ) ;
#144688=ORIENTED_EDGE ( 'NONE', *, *, #92489, .F. ) ;
#144922=AXIS2_PLACEMENT_3D ( 'NONE', #95580, #80363, #143275 ) ;
#145021=LINE ( 'NONE', #129883, #124426 ) ;
#145271=ORIENTED_EDGE ( 'NONE', *, *, #213625, .T. ) ;
#145525=ADVANCED_FACE ( 'NONE', ( #154866 ), #57361, .T. ) ;
#145607=EDGE_CURVE ( 'NONE', #112521, #188607, #59485, .T. ) ;
#145707=EDGE_CURVE ( 'NONE', #96482, #122450, #42198, .T. ) ;
#146301=ORIENTED_EDGE ( 'NONE', *, *, #11886, .F. ) ;
#146486=DIRECTION ( 'NONE',  ( 0.000000000000000000, 0.000000000000000000, 1.000000000000000000 ) ) ;
#146519=ORIENTED_EDGE ( 'NONE', *, *, #152411, .F. ) ;
#146685=ORIENTED_EDGE ( 'NONE', *, *, #209914, .F. ) ;
#146731=EDGE_LOOP ( 'NONE', ( #185900, #208039, #175866, #89894, #184465, #100920, #77275, #48167, #75048, #6914, #177441, #144688 ) ) ;
#146916=DIRECTION ( 'NONE',  ( 0.000000000000000000, 1.000000000000000000, 0.000000000000000000 ) ) ;
#147117=CARTESIAN_POINT ( 'NONE',  ( 4.000000000000012434, 0.000000000000000000, 0.7500000000000006661 ) ) ;
#147380=LINE ( 'NONE', #181977, #11226 ) ;
#147600=DIRECTION ( 'NONE',  ( 0.000000000000000000, 1.000000000000000000, 0.000000000000000000 ) ) ;
#148101=ORIENTED_EDGE ( 'NONE', *, *, #204535, .F. ) ;
#148132=ORIENTED_EDGE ( 'NONE', *, *, #185183, .F. ) ;
#148435=ORIENTED_EDGE ( 'NONE', *, *, #111829, .T. ) ;
#148490=CARTESIAN_POINT ( 'NONE',  ( -3.929058411375401683, 5.999999999999998224, -0.7500000000000006661 ) ) ;
#149003=ORIENTED_EDGE ( 'NONE', *, *, #88556, .F. ) ;
#149140=EDGE_CURVE ( 'NONE', #65271, #11614, #76641, .T. ) ;
#149503=CIRCLE ( 'NONE', #69992, 4.000000000000000000 ) ;
#149562=CARTESIAN_POINT ( 'NONE',  ( 0.000000000000000000, 5.999999999999998224, 0.000000000000000000 ) ) ;
#149799=VECTOR ( 'NONE', #164049, 1000.000000000000000 ) ;
#150282=EDGE_LOOP ( 'NONE', ( #211758, #76502, #205403, #104717 ) ) ;
#150288=DIRECTION ( 'NONE',  ( -1.000000000000000000, 0.000000000000000000, 0.000000000000000000 ) ) ;
#150361=DIRECTION ( 'NONE',  ( -0.000000000000000000, -1.000000000000000000, -0.000000000000000000 ) ) ;
#150402=EDGE_CURVE ( 'NONE', #159873, #125532, #85472, .T. ) ;
#150506=SURFACE_STYLE_FILL_AREA ( #18336 ) ;
#150694=CARTESIAN_POINT ( 'NONE',  ( 0.000000000000000000, 4.999999999999997335, 0.000000000000000000 ) ) ;
#150713=VECTOR ( 'NONE', #197735, 1000.000000000000000 ) ;
#150802=ORIENTED_EDGE ( 'NONE', *, *, #133443, .F. ) ;
#151332=ORIENTED_EDGE ( 'NONE', *, *, #164982, .F. ) ;
#151904=( GEOMETRIC_REPRESENTATION_CONTEXT ( 3 ) GLOBAL_UNCERTAINTY_ASSIGNED_CONTEXT ( ( #122240 ) ) GLOBAL_UNIT_ASSIGNED_CONTEXT ( ( #116833, #166598, #18187 ) ) REPRESENTATION_CONTEXT ( 'NONE', 'WORKASPACE' ) );
#152111=AXIS2_PLACEMENT_3D ( 'NONE', #8096, #171666, #174904 ) ;
#152334=CARTESIAN_POINT ( 'NONE',  ( 4.000000000000012434, 6.499999999999999112, -0.7500000000000006661 ) ) ;
#152411=EDGE_CURVE ( 'NONE', #4753, #88429, #44359, .T. ) ;
#152541=ORIENTED_EDGE ( 'NONE', *, *, #181995, .T. ) ;
#152649=LINE ( 'NONE', #80202, #91869 ) ;
#152808=DIRECTION ( 'NONE',  ( 0.000000000000000000, 1.000000000000000000, 0.000000000000000000 ) ) ;
#153056=CIRCLE ( 'NONE', #135752, 4.000000000000000000 ) ;
#153647=VECTOR ( 'NONE', #25526, 1000.000000000000000 ) ;
#153689=ORIENTED_EDGE ( 'NONE', *, *, #174645, .F. ) ;
#154020=ORIENTED_EDGE ( 'NONE', *, *, #157920, .F. ) ;
#154520=AXIS2_PLACEMENT_3D ( 'NONE', #173453, #203767, #54354 ) ;
#154550=LINE ( 'NONE', #87416, #119720 ) ;
#154866=FACE_OUTER_BOUND ( 'NONE', #113466, .T. ) ;
#154959=VECTOR ( 'NONE', #16565, 1000.000000000000000 ) ;
#155153=AXIS2_PLACEMENT_3D ( 'NONE', #72496, #93055, #10693 ) ;
#155372=DIRECTION ( 'NONE',  ( 0.000000000000000000, 1.000000000000000000, 0.000000000000000000 ) ) ;
#155934=CARTESIAN_POINT ( 'NONE',  ( -3.929058411375401683, -1.000000000000000888, -0.7500000000000006661 ) ) ;
#156391=CARTESIAN_POINT ( 'NONE',  ( 4.000000000000012434, 0.000000000000000000, -0.7500000000000006661 ) ) ;
#156462=AXIS2_PLACEMENT_3D ( 'NONE', #129764, #195747, #47384 ) ;
#156566=VERTEX_POINT ( 'NONE', #177157 ) ;
#156740=ORIENTED_EDGE ( 'NONE', *, *, #32247, .T. ) ;
#156896=EDGE_CURVE ( 'NONE', #162364, #205873, #115705, .T. ) ;
#156984=AXIS2_PLACEMENT_3D ( 'NONE', #150694, #152808, #52114 ) ;
#157246=DIRECTION ( 'NONE',  ( 0.000000000000000000, 1.000000000000000000, -0.000000000000000000 ) ) ;
#157255=CARTESIAN_POINT ( 'NONE',  ( 4.000000000000012434, 0.000000000000000000, -0.7500000000000006661 ) ) ;
#157920=EDGE_CURVE ( 'NONE', #49683, #42393, #145021, .T. ) ;
#158405=AXIS2_PLACEMENT_3D ( 'NONE', #92262, #126949, #60790 ) ;
#159073=CARTESIAN_POINT ( 'NONE',  ( -1.854049621773913525, 5.499999999999998224, 0.7500000000000006661 ) ) ;
#159373=DIRECTION ( 'NONE',  ( -1.000000000000000000, 0.000000000000000000, 0.000000000000000000 ) ) ;
#159581=DIRECTION ( 'NONE',  ( 0.000000000000000000, 0.000000000000000000, -1.000000000000000000 ) ) ;
#159873=VERTEX_POINT ( 'NONE', #132706 ) ;
#160021=AXIS2_PLACEMENT_3D ( 'NONE', #157255, #43515, #144244 ) ;
#160220=DIRECTION ( 'NONE',  ( 0.000000000000000000, 0.000000000000000000, 1.000000000000000000 ) ) ;
#160336=VERTEX_POINT ( 'NONE', #159073 ) ;
#160545=FACE_OUTER_BOUND ( 'NONE', #15855, .T. ) ;
#160725=DIRECTION ( 'NONE',  ( 0.000000000000000000, 0.000000000000000000, 1.000000000000000000 ) ) ;
#160813=AXIS2_PLACEMENT_3D ( 'NONE', #147117, #111470, #12810 ) ;
#160911=DIRECTION ( 'NONE',  ( 0.000000000000000000, 1.000000000000000000, 0.000000000000000000 ) ) ;
#161216=ORIENTED_EDGE ( 'NONE', *, *, #171344, .F. ) ;
#161264=VECTOR ( 'NONE', #73336, 1000.000000000000000 ) ;
#161266=DIRECTION ( 'NONE',  ( 1.000000000000000000, 0.000000000000000000, 0.000000000000000000 ) ) ;
#162364=VERTEX_POINT ( 'NONE', #80503 ) ;
#162671=ORIENTED_EDGE ( 'NONE', *, *, #64463, .T. ) ;
#162677=ORIENTED_EDGE ( 'NONE', *, *, #118655, .F. ) ;
#163094=VECTOR ( 'NONE', #201566, 1000.000000000000000 ) ;
#163798=AXIS2_PLACEMENT_3D ( 'NONE', #5753, #85977, #102226 ) ;
#163875=EDGE_CURVE ( 'NONE', #69052, #120928, #97271, .T. ) ;
#163882=ORIENTED_EDGE ( 'NONE', *, *, #59071, .F. ) ;
#164049=DIRECTION ( 'NONE',  ( 0.000000000000000000, 1.000000000000000000, -0.000000000000000000 ) ) ;
#164115=ADVANCED_FACE ( 'NONE', ( #5816, #72968 ), #38351, .F. ) ;
#164151=VECTOR ( 'NONE', #193176, 1000.000000000000000 ) ;
#164665=DIRECTION ( 'NONE',  ( 0.000000000000000000, 1.000000000000000000, 0.000000000000000000 ) ) ;
#164982=EDGE_CURVE ( 'NONE', #156566, #85656, #200975, .T. ) ;
#165523=SHAPE_REPRESENTATION_RELATIONSHIP ( 'NONE' , 'NONE' ,  #47273, #88981 ) ;
#165712=PLANE ( 'NONE',  #166518 ) ;
#165721=DIRECTION ( 'NONE',  ( -1.000000000000000000, 0.000000000000000000, 0.000000000000000000 ) ) ;
#166027=ADVANCED_FACE ( 'NONE', ( #99645 ), #165712, .F. ) ;
#166283=VERTEX_POINT ( 'NONE', #191531 ) ;
#166518=AXIS2_PLACEMENT_3D ( 'NONE', #17301, #183018, #67108 ) ;
#166585=ORIENTED_EDGE ( 'NONE', *, *, #1086, .T. ) ;
#166598=( NAMED_UNIT ( * ) PLANE_ANGLE_UNIT ( ) SI_UNIT ( $, .RADIAN. ) );
#166600=CARTESIAN_POINT ( 'NONE',  ( 3.449547071718272573, -1.000000000000000888, -2.024999999999992806 ) ) ;
#166659=LINE ( 'NONE', #1986, #173559 ) ;
#166839=DIRECTION ( 'NONE',  ( -0.000000000000000000, -1.000000000000000000, 0.000000000000000000 ) ) ;
#167316=ORIENTED_EDGE ( 'NONE', *, *, #163875, .F. ) ;
#167502=CARTESIAN_POINT ( 'NONE',  ( 0.000000000000000000, 6.499999999999999112, 0.000000000000000000 ) ) ;
#167695=FACE_OUTER_BOUND ( 'NONE', #794, .T. ) ;
#168316=ADVANCED_FACE ( 'NONE', ( #15193 ), #47745, .F. ) ;
#170295=ORIENTED_EDGE ( 'NONE', *, *, #213625, .F. ) ;
#171024=LINE ( 'NONE', #138543, #144281 ) ;
#171038=DIRECTION ( 'NONE',  ( -1.000000000000000000, 0.000000000000000000, 0.000000000000000000 ) ) ;
#171057=ORIENTED_EDGE ( 'NONE', *, *, #136186, .F. ) ;
#171097=ORIENTED_EDGE ( 'NONE', *, *, #95578, .F. ) ;
#171295=VECTOR ( 'NONE', #88960, 1000.000000000000000 ) ;
#171344=EDGE_CURVE ( 'NONE', #175693, #65271, #198703, .T. ) ;
#171569=ORIENTED_EDGE ( 'NONE', *, *, #29580, .T. ) ;
#171666=DIRECTION ( 'NONE',  ( -0.000000000000000000, -1.000000000000000000, 0.000000000000000000 ) ) ;
#171816=CARTESIAN_POINT ( 'NONE',  ( 0.000000000000000000, 7.500000000000000000, -1.500000000000000222 ) ) ;
#171842=ORIENTED_EDGE ( 'NONE', *, *, #145707, .F. ) ;
#172089=ADVANCED_FACE ( 'NONE', ( #190357 ), #108128, .T. ) ;
#172851=CARTESIAN_POINT ( 'NONE',  ( 4.000000000000012434, 0.000000000000000000, 0.7500000000000006661 ) ) ;
#173079=EDGE_LOOP ( 'NONE', ( #167316, #136607, #195077, #67292, #51118, #34299, #118153 ) ) ;
#173358=AXIS2_PLACEMENT_3D ( 'NONE', #40503, #107691, #88172 ) ;
#173453=CARTESIAN_POINT ( 'NONE',  ( 4.000000000000012434, 0.000000000000000000, 0.7500000000000006661 ) ) ;
#173510=LINE ( 'NONE', #25083, #212530 ) ;
#173559=VECTOR ( 'NONE', #86472, 1000.000000000000000 ) ;
#173738=EDGE_LOOP ( 'NONE', ( #76581, #96662, #125868, #70156 ) ) ;
#174227=CIRCLE ( 'NONE', #122346, 4.000000000000000000 ) ;
#174333=DIRECTION ( 'NONE',  ( -0.000000000000000000, -1.000000000000000000, -0.000000000000000000 ) ) ;
#174535=EDGE_CURVE ( 'NONE', #175693, #142172, #153056, .T. ) ;
#174577=DIRECTION ( 'NONE',  ( -1.000000000000000000, 0.000000000000000000, 0.000000000000000000 ) ) ;
#174607=PLANE ( 'NONE',  #112556 ) ;
#174645=EDGE_CURVE ( 'NONE', #85656, #156566, #73422, .T. ) ;
#174801=EDGE_CURVE ( 'NONE', #99756, #11614, #64051, .T. ) ;
#174904=DIRECTION ( 'NONE',  ( 0.000000000000000000, 0.000000000000000000, -1.000000000000000000 ) ) ;
#175034=EDGE_CURVE ( 'NONE', #108790, #166283, #149503, .T. ) ;
#175365=FACE_OUTER_BOUND ( 'NONE', #85284, .T. ) ;
#175693=VERTEX_POINT ( 'NONE', #44355 ) ;
#175866=ORIENTED_EDGE ( 'NONE', *, *, #152411, .T. ) ;
#175922=DIRECTION ( 'NONE',  ( 0.000000000000000000, 1.000000000000000000, 0.000000000000000000 ) ) ;
#176299=DIRECTION ( 'NONE',  ( 0.000000000000000000, 1.000000000000000000, 0.000000000000000000 ) ) ;
#176691=PLANE ( 'NONE',  #160021 ) ;
#177157=CARTESIAN_POINT ( 'NONE',  ( 0.000000000000000000, 0.000000000000000000, -2.000000000000000000 ) ) ;
#177174=ORIENTED_EDGE ( 'NONE', *, *, #118655, .T. ) ;
#177400=ORIENTED_EDGE ( 'NONE', *, *, #204911, .T. ) ;
#177441=ORIENTED_EDGE ( 'NONE', *, *, #142583, .T. ) ;
#177648=ORIENTED_EDGE ( 'NONE', *, *, #150402, .F. ) ;
#177874=ADVANCED_FACE ( 'NONE', ( #141038 ), #176691, .T. ) ;
#178101=EDGE_CURVE ( 'NONE', #144460, #58716, #83440, .T. ) ;
#178334=EDGE_LOOP ( 'NONE', ( #93309, #193675, #97596, #190496, #72119, #80450, #64178, #131908, #32030, #7909, #194124, #195080 ) ) ;
#179332=CARTESIAN_POINT ( 'NONE',  ( 0.000000000000000000, 5.999999999999998224, 0.000000000000000000 ) ) ;
#179576=ORIENTED_EDGE ( 'NONE', *, *, #157920, .T. ) ;
#179635=CARTESIAN_POINT ( 'NONE',  ( 0.000000000000000000, 6.499999999999999112, 0.000000000000000000 ) ) ;
#179823=LINE ( 'NONE', #15160, #59877 ) ;
#179963=EDGE_CURVE ( 'NONE', #205873, #94313, #191824, .T. ) ;
#180119=VERTEX_POINT ( 'NONE', #82358 ) ;
#181457=EDGE_CURVE ( 'NONE', #160336, #213592, #50070, .T. ) ;
#181573=ORIENTED_EDGE ( 'NONE', *, *, #185183, .T. ) ;
#181708=FACE_OUTER_BOUND ( 'NONE', #57553, .T. ) ;
#181779=ORIENTED_EDGE ( 'NONE', *, *, #88556, .T. ) ;
#181977=CARTESIAN_POINT ( 'NONE',  ( 2.449293598294706414E-16, 5.499999999999998224, 2.000000000000000000 ) ) ;
#181995=EDGE_CURVE ( 'NONE', #86578, #205093, #187660, .T. ) ;
#182203=DIRECTION ( 'NONE',  ( 0.000000000000000000, 0.000000000000000000, 1.000000000000000000 ) ) ;
#182227=EDGE_LOOP ( 'NONE', ( #141237, #76871, #192306, #161216 ) ) ;
#182547=EDGE_CURVE ( 'NONE', #14623, #68331, #81384, .T. ) ;
#183018=DIRECTION ( 'NONE',  ( 0.000000000000000000, 0.000000000000000000, -1.000000000000000000 ) ) ;
#183110=STYLED_ITEM ( 'NONE', ( #184954 ), #88981 ) ;
#183173=LINE ( 'NONE', #16386, #2981 ) ;
#183267=DIRECTION ( 'NONE',  ( -0.000000000000000000, -1.000000000000000000, 0.000000000000000000 ) ) ;
#184039=SURFACE_STYLE_USAGE ( .BOTH. , #52979 ) ;
#184320=ORIENTED_EDGE ( 'NONE', *, *, #45609, .T. ) ;
#184465=ORIENTED_EDGE ( 'NONE', *, *, #82581, .F. ) ;
#184540=AXIS2_PLACEMENT_3D ( 'NONE', #212651, #175922, #160725 ) ;
#184954=PRESENTATION_STYLE_ASSIGNMENT (( #69065 ) ) ;
#185107=DIRECTION ( 'NONE',  ( 0.000000000000000000, 0.000000000000000000, 1.000000000000000000 ) ) ;
#185183=EDGE_CURVE ( 'NONE', #162364, #84441, #124197, .T. ) ;
#185742=ADVANCED_FACE ( 'NONE', ( #190992 ), #209370, .T. ) ;
#185900=ORIENTED_EDGE ( 'NONE', *, *, #44124, .T. ) ;
#186026=FILL_AREA_STYLE_COLOUR ( '', #68982 ) ;
#186064=CARTESIAN_POINT ( 'NONE',  ( 0.000000000000000000, 4.999999999999997335, 0.000000000000000000 ) ) ;
#186552=CARTESIAN_POINT ( 'NONE',  ( 3.449547071718269020, 5.499999999999998224, -2.024999999999999023 ) ) ;
#186725=DIRECTION ( 'NONE',  ( 0.000000000000000000, 0.000000000000000000, 1.000000000000000000 ) ) ;
#187288=PRODUCT_DEFINITION_CONTEXT ( 'detailed design', #40891, 'design' ) ;
#187306=ORIENTED_EDGE ( 'NONE', *, *, #182547, .T. ) ;
#187660=LINE ( 'NONE', #101076, #42816 ) ;
#188078=ORIENTED_EDGE ( 'NONE', *, *, #174801, .F. ) ;
#188103=AXIS2_PLACEMENT_3D ( 'NONE', #156391, #159581, #42658 ) ;
#188607=VERTEX_POINT ( 'NONE', #96227 ) ;
#189028=AXIS2_PLACEMENT_3D ( 'NONE', #89325, #155372, #6957 ) ;
#189103=CARTESIAN_POINT ( 'NONE',  ( 1.854049621773927514, 5.499999999999998224, -0.7500000000000006661 ) ) ;
#189820=FACE_OUTER_BOUND ( 'NONE', #150282, .T. ) ;
#190357=FACE_OUTER_BOUND ( 'NONE', #77505, .T. ) ;
#190496=ORIENTED_EDGE ( 'NONE', *, *, #45609, .F. ) ;
#190524=CARTESIAN_POINT ( 'NONE',  ( -3.929058411375426108, -1.000000000000000888, 0.7499999999999988898 ) ) ;
#190690=LINE ( 'NONE', #123672, #171295 ) ;
#190875=DIRECTION ( 'NONE',  ( -1.000000000000000000, 0.000000000000000000, 0.000000000000000000 ) ) ;
#190992=FACE_OUTER_BOUND ( 'NONE', #207143, .T. ) ;
#191028=CARTESIAN_POINT ( 'NONE',  ( 4.000000000000012434, 5.499999999999998224, -0.7500000000000006661 ) ) ;
#191503=VECTOR ( 'NONE', #211371, 1000.000000000000000 ) ;
#191531=CARTESIAN_POINT ( 'NONE',  ( 3.449547071718272573, 5.999999999999998224, -2.024999999999992806 ) ) ;
#191824=CIRCLE ( 'NONE', #91522, 2.000000000000000000 ) ;
#191961=EDGE_CURVE ( 'NONE', #79391, #105851, #46194, .T. ) ;
#192306=ORIENTED_EDGE ( 'NONE', *, *, #149140, .F. ) ;
#192633=LINE ( 'NONE', #56261, #50110 ) ;
#193176=DIRECTION ( 'NONE',  ( -1.000000000000000000, 0.000000000000000000, 0.000000000000000000 ) ) ;
#193328=CIRCLE ( 'NONE', #99947, 2.000000000000000000 ) ;
#193675=ORIENTED_EDGE ( 'NONE', *, *, #45482, .F. ) ;
#194084=VERTEX_POINT ( 'NONE', #7624 ) ;
#194104=PLANE ( 'NONE',  #144922 ) ;
#194124=ORIENTED_EDGE ( 'NONE', *, *, #195348, .T. ) ;
#194651=CARTESIAN_POINT ( 'NONE',  ( 3.929058411375439874, 5.999999999999998224, -0.7500000000000006661 ) ) ;
#195077=ORIENTED_EDGE ( 'NONE', *, *, #156896, .T. ) ;
#195080=ORIENTED_EDGE ( 'NONE', *, *, #136902, .T. ) ;
#195157=ORIENTED_EDGE ( 'NONE', *, *, #164982, .T. ) ;
#195348=EDGE_CURVE ( 'NONE', #122450, #49683, #88702, .T. ) ;
#195747=DIRECTION ( 'NONE',  ( 0.000000000000000000, 1.000000000000000000, 0.000000000000000000 ) ) ;
#196145=VECTOR ( 'NONE', #204258, 1000.000000000000000 ) ;
#196170=ADVANCED_FACE ( 'NONE', ( #12605 ), #97099, .T. ) ;
#196275=VECTOR ( 'NONE', #77846, 1000.000000000000000 ) ;
#196519=ORIENTED_EDGE ( 'NONE', *, *, #178101, .F. ) ;
#196536=CARTESIAN_POINT ( 'NONE',  ( 3.929058411375439874, -1.000000000000000888, -0.7500000000000006661 ) ) ;
#197580=VECTOR ( 'NONE', #84971, 1000.000000000000000 ) ;
#197636=AXIS2_PLACEMENT_3D ( 'NONE', #179332, #73535, #141788 ) ;
#197735=DIRECTION ( 'NONE',  ( 0.000000000000000000, 1.000000000000000000, 0.000000000000000000 ) ) ;
#198014=LINE ( 'NONE', #166600, #9759 ) ;
#198562=DIRECTION ( 'NONE',  ( 0.000000000000000000, 0.000000000000000000, 1.000000000000000000 ) ) ;
#198703=LINE ( 'NONE', #37289, #197580 ) ;
#198875=EDGE_LOOP ( 'NONE', ( #7753, #171569, #181779, #33297 ) ) ;
#198949=EDGE_CURVE ( 'NONE', #69052, #162364, #4983, .T. ) ;
#199887=CARTESIAN_POINT ( 'NONE',  ( 0.000000000000000000, 5.999999999999998224, 0.000000000000000000 ) ) ;
#200407=AXIS2_PLACEMENT_3D ( 'NONE', #95216, #132002, #161266 ) ;
#200417=DIRECTION ( 'NONE',  ( 0.000000000000000000, 1.000000000000000000, 0.000000000000000000 ) ) ;
#200975=CIRCLE ( 'NONE', #21154, 2.000000000000000000 ) ;
#201380=EDGE_CURVE ( 'NONE', #88429, #71979, #132736, .T. ) ;
#201566=DIRECTION ( 'NONE',  ( -1.000000000000000000, 0.000000000000000000, 0.000000000000000000 ) ) ;
#201712=LINE ( 'NONE', #17627, #154959 ) ;
#202400=CIRCLE ( 'NONE', #116056, 4.000000000000000000 ) ;
#202760=ADVANCED_FACE ( 'NONE', ( #43517 ), #44580, .T. ) ;
#203035=DIRECTION ( 'NONE',  ( 0.000000000000000000, 0.000000000000000000, 1.000000000000000000 ) ) ;
#203288=CARTESIAN_POINT ( 'NONE',  ( 3.929058411375439874, -1.000000000000000888, 0.7500000000000006661 ) ) ;
#203333=FACE_OUTER_BOUND ( 'NONE', #173738, .T. ) ;
#203767=DIRECTION ( 'NONE',  ( 0.000000000000000000, 0.000000000000000000, -1.000000000000000000 ) ) ;
#204096=CARTESIAN_POINT ( 'NONE',  ( -3.929058411375426108, 6.499999999999999112, 0.7499999999999988898 ) ) ;
#204258=DIRECTION ( 'NONE',  ( -1.000000000000000000, 0.000000000000000000, 0.000000000000000000 ) ) ;
#204531=EDGE_LOOP ( 'NONE', ( #43091, #136857, #2364, #115177, #119995, #152541, #127593, #113938 ) ) ;
#204535=EDGE_CURVE ( 'NONE', #166283, #105851, #183173, .T. ) ;
#204734=VECTOR ( 'NONE', #209116, 1000.000000000000000 ) ;
#204911=EDGE_CURVE ( 'NONE', #142172, #144460, #53769, .T. ) ;
#205093=VERTEX_POINT ( 'NONE', #122055 ) ;
#205172=CARTESIAN_POINT ( 'NONE',  ( 2.449293598294706414E-16, 5.499999999999998224, 2.000000000000000000 ) ) ;
#205403=ORIENTED_EDGE ( 'NONE', *, *, #116869, .F. ) ;
#205713=CARTESIAN_POINT ( 'NONE',  ( -1.854049621773913525, 4.999999999999997335, 0.7500000000000006661 ) ) ;
#205873=VERTEX_POINT ( 'NONE', #33110 ) ;
#206082=VECTOR ( 'NONE', #171038, 1000.000000000000000 ) ;
#206477=VERTEX_POINT ( 'NONE', #204096 ) ;
#206639=DIRECTION ( 'NONE',  ( 0.000000000000000000, 0.000000000000000000, 1.000000000000000000 ) ) ;
#206776=CARTESIAN_POINT ( 'NONE',  ( 4.000000000000012434, 4.999999999999997335, 0.7500000000000006661 ) ) ;
#207118=CARTESIAN_POINT ( 'NONE',  ( 2.449293598294706414E-16, 0.000000000000000000, 2.000000000000000000 ) ) ;
#207143=EDGE_LOOP ( 'NONE', ( #73306, #76457, #115324, #2458 ) ) ;
#207764=CARTESIAN_POINT ( 'NONE',  ( 1.299038105676669330, 5.999999999999998224, 0.7500000000000006661 ) ) ;
#207943=VERTEX_POINT ( 'NONE', #56775 ) ;
#208039=ORIENTED_EDGE ( 'NONE', *, *, #48666, .T. ) ;
#208738=DIRECTION ( 'NONE',  ( 0.000000000000000000, 1.000000000000000000, 0.000000000000000000 ) ) ;
#208878=DIRECTION ( 'NONE',  ( 0.000000000000000000, -1.000000000000000000, 0.000000000000000000 ) ) ;
#208944=DIRECTION ( 'NONE',  ( 0.000000000000000000, 1.000000000000000000, 0.000000000000000000 ) ) ;
#209116=DIRECTION ( 'NONE',  ( 0.000000000000000000, 1.000000000000000000, 0.000000000000000000 ) ) ;
#209156=CARTESIAN_POINT ( 'NONE',  ( 4.000000000000012434, 4.999999999999997335, -0.7500000000000006661 ) ) ;
#209370=PLANE ( 'NONE',  #188103 ) ;
#209626=DIRECTION ( 'NONE',  ( -0.000000000000000000, -1.000000000000000000, 0.000000000000000000 ) ) ;
#209914=EDGE_CURVE ( 'NONE', #180119, #86578, #82311, .T. ) ;
#210011=CARTESIAN_POINT ( 'NONE',  ( 0.000000000000000000, 5.999999999999998224, 0.000000000000000000 ) ) ;
#211259=CARTESIAN_POINT ( 'NONE',  ( -3.929058411375426108, -1.000000000000000888, 0.7499999999999988898 ) ) ;
#211371=DIRECTION ( 'NONE',  ( -1.000000000000000000, 0.000000000000000000, 0.000000000000000000 ) ) ;
#211476=ADVANCED_FACE ( 'NONE', ( #175365 ), #26947, .T. ) ;
#211758=ORIENTED_EDGE ( 'NONE', *, *, #118355, .T. ) ;
#212000=CARTESIAN_POINT ( 'NONE',  ( 0.000000000000000000, -1.000000000000000888, 0.000000000000000000 ) ) ;
#212162=ORIENTED_EDGE ( 'NONE', *, *, #97896, .F. ) ;
#212185=CARTESIAN_POINT ( 'NONE',  ( 0.000000000000000000, 0.000000000000000000, 0.000000000000000000 ) ) ;
#212530=VECTOR ( 'NONE', #157246, 1000.000000000000000 ) ;
#212651=CARTESIAN_POINT ( 'NONE',  ( 4.000000000000012434, 5.999999999999998224, -1.214306433183764966E-14 ) ) ;
#212686=CARTESIAN_POINT ( 'NONE',  ( 0.000000000000000000, 5.499999999999998224, 0.000000000000000000 ) ) ;
#213106=CARTESIAN_POINT ( 'NONE',  ( -3.449547071718232605, 5.999999999999998224, -2.024999999999999911 ) ) ;
#213592=VERTEX_POINT ( 'NONE', #205172 ) ;
#213625=EDGE_CURVE ( 'NONE', #213592, #42393, #193328, .T. ) ;
#213798=VERTEX_POINT ( 'NONE', #31534 ) ;
#213937=ORIENTED_EDGE ( 'NONE', *, *, #11640, .T. ) ;
#213993=PRODUCT_CONTEXT ( 'NONE', #104451, 'mechanical' ) ;
ENDSEC;
END-ISO-10303-21;
